ISO-10303-21;
HEADER;
/* Generated by software containing ST-Developer
 * from STEP Tools, Inc. (www.steptools.com) 
 */

FILE_DESCRIPTION(
/* description */ ('Worm-less right-angle friction wheel drive'),
/* implementation_level */ '2;1');

FILE_NAME(
/* name */ 'Bearing cap (7).step',
/* time_stamp */ '2026-10-28T03:22:36-07:00',
/* author */ (''),
/* organization */ (''),
/* preprocessor_version */ 'ST-DEVELOPER v20.2',
/* originating_system */ 'Autodesk Translation Framework v15.17.0.0',
/* authorisation */ '');

FILE_SCHEMA (('AUTOMOTIVE_DESIGN { 1 0 10303 214 3 1 1 }'));
ENDSEC;

DATA;
#10=MECHANICAL_DESIGN_GEOMETRIC_PRESENTATION_REPRESENTATION('',(#626),#17046);
#532=SHAPE_REPRESENTATION_RELATIONSHIP('SRR','None',#17275,#579);
#579=ADVANCED_BREP_SHAPE_REPRESENTATION('',(#680),#17011);
#626=STYLED_ITEM('',(#17591),#680);
#680=MANIFOLD_SOLID_BREP('Body1',#8181);
#884=FACE_BOUND('',#2041,.T.);
#885=FACE_BOUND('',#2045,.T.);
#886=FACE_BOUND('',#2046,.T.);
#887=FACE_BOUND('',#2047,.T.);
#888=FACE_BOUND('',#2048,.T.);
#889=FACE_BOUND('',#2049,.T.);
#890=FACE_BOUND('',#2051,.T.);
#891=FACE_BOUND('',#2052,.T.);
#892=FACE_BOUND('',#2053,.T.);
#893=FACE_BOUND('',#2054,.T.);
#894=FACE_BOUND('',#2055,.T.);
#1045=PLANE('',#9165);
#1046=PLANE('',#9172);
#1047=PLANE('',#9173);
#1400=FACE_OUTER_BOUND('',#2035,.T.);
#1401=FACE_OUTER_BOUND('',#2036,.T.);
#1402=FACE_OUTER_BOUND('',#2037,.T.);
#1403=FACE_OUTER_BOUND('',#2038,.T.);
#1404=FACE_OUTER_BOUND('',#2039,.T.);
#1405=FACE_OUTER_BOUND('',#2040,.T.);
#1406=FACE_OUTER_BOUND('',#2042,.T.);
#1407=FACE_OUTER_BOUND('',#2043,.T.);
#1408=FACE_OUTER_BOUND('',#2044,.T.);
#1409=FACE_OUTER_BOUND('',#2050,.T.);
#2035=EDGE_LOOP('',(#6464,#6465,#6466,#6467));
#2036=EDGE_LOOP('',(#6468,#6469,#6470,#6471));
#2037=EDGE_LOOP('',(#6472,#6473,#6474,#6475));
#2038=EDGE_LOOP('',(#6476,#6477,#6478,#6479));
#2039=EDGE_LOOP('',(#6480,#6481,#6482,#6483));
#2040=EDGE_LOOP('',(#6484));
#2041=EDGE_LOOP('',(#6485));
#2042=EDGE_LOOP('',(#6486,#6487,#6488,#6489));
#2043=EDGE_LOOP('',(#6490,#6491,#6492,#6493));
#2044=EDGE_LOOP('',(#6494));
#2045=EDGE_LOOP('',(#6495));
#2046=EDGE_LOOP('',(#6496));
#2047=EDGE_LOOP('',(#6497));
#2048=EDGE_LOOP('',(#6498));
#2049=EDGE_LOOP('',(#6499));
#2050=EDGE_LOOP('',(#6500));
#2051=EDGE_LOOP('',(#6501));
#2052=EDGE_LOOP('',(#6502));
#2053=EDGE_LOOP('',(#6503));
#2054=EDGE_LOOP('',(#6504));
#2055=EDGE_LOOP('',(#6505));
#2644=LINE('',#13364,#3184);
#2645=LINE('',#13370,#3185);
#2646=LINE('',#13376,#3186);
#2647=LINE('',#13382,#3187);
#2648=LINE('',#13388,#3188);
#2649=LINE('',#13396,#3189);
#2650=LINE('',#13401,#3190);
#3184=VECTOR('',#10860,0.225);
#3185=VECTOR('',#10867,0.225);
#3186=VECTOR('',#10874,0.225);
#3187=VECTOR('',#10881,0.225);
#3188=VECTOR('',#10888,1.59);
#3189=VECTOR('',#10899,1.2);
#3190=VECTOR('',#10904,2.4);
#3655=CIRCLE('',#9151,0.225);
#3656=CIRCLE('',#9152,0.225);
#3657=CIRCLE('',#9154,0.225);
#3658=CIRCLE('',#9155,0.225);
#3659=CIRCLE('',#9157,0.225);
#3660=CIRCLE('',#9158,0.225);
#3661=CIRCLE('',#9160,0.225);
#3662=CIRCLE('',#9161,0.225);
#3663=CIRCLE('',#9163,1.59);
#3664=CIRCLE('',#9164,1.59);
#3665=CIRCLE('',#9166,1.2);
#3666=CIRCLE('',#9168,1.2);
#3667=CIRCLE('',#9170,2.4);
#3668=CIRCLE('',#9171,2.4);
#4179=VERTEX_POINT('',#13361);
#4180=VERTEX_POINT('',#13363);
#4181=VERTEX_POINT('',#13367);
#4182=VERTEX_POINT('',#13369);
#4183=VERTEX_POINT('',#13373);
#4184=VERTEX_POINT('',#13375);
#4185=VERTEX_POINT('',#13379);
#4186=VERTEX_POINT('',#13381);
#4187=VERTEX_POINT('',#13385);
#4188=VERTEX_POINT('',#13387);
#4189=VERTEX_POINT('',#13391);
#4190=VERTEX_POINT('',#13394);
#4191=VERTEX_POINT('',#13398);
#4192=VERTEX_POINT('',#13400);
#5001=EDGE_CURVE('',#4179,#4179,#3655,.T.);
#5002=EDGE_CURVE('',#4179,#4180,#2644,.T.);
#5003=EDGE_CURVE('',#4180,#4180,#3656,.T.);
#5004=EDGE_CURVE('',#4181,#4181,#3657,.T.);
#5005=EDGE_CURVE('',#4181,#4182,#2645,.T.);
#5006=EDGE_CURVE('',#4182,#4182,#3658,.T.);
#5007=EDGE_CURVE('',#4183,#4183,#3659,.T.);
#5008=EDGE_CURVE('',#4183,#4184,#2646,.T.);
#5009=EDGE_CURVE('',#4184,#4184,#3660,.T.);
#5010=EDGE_CURVE('',#4185,#4185,#3661,.T.);
#5011=EDGE_CURVE('',#4185,#4186,#2647,.T.);
#5012=EDGE_CURVE('',#4186,#4186,#3662,.T.);
#5013=EDGE_CURVE('',#4187,#4187,#3663,.T.);
#5014=EDGE_CURVE('',#4187,#4188,#2648,.T.);
#5015=EDGE_CURVE('',#4188,#4188,#3664,.T.);
#5016=EDGE_CURVE('',#4189,#4189,#3665,.T.);
#5017=EDGE_CURVE('',#4190,#4190,#3666,.T.);
#5018=EDGE_CURVE('',#4190,#4189,#2649,.T.);
#5019=EDGE_CURVE('',#4191,#4191,#3667,.T.);
#5020=EDGE_CURVE('',#4191,#4192,#2650,.T.);
#5021=EDGE_CURVE('',#4192,#4192,#3668,.T.);
#6464=ORIENTED_EDGE('',*,*,#5001,.F.);
#6465=ORIENTED_EDGE('',*,*,#5002,.T.);
#6466=ORIENTED_EDGE('',*,*,#5003,.F.);
#6467=ORIENTED_EDGE('',*,*,#5002,.F.);
#6468=ORIENTED_EDGE('',*,*,#5004,.F.);
#6469=ORIENTED_EDGE('',*,*,#5005,.T.);
#6470=ORIENTED_EDGE('',*,*,#5006,.F.);
#6471=ORIENTED_EDGE('',*,*,#5005,.F.);
#6472=ORIENTED_EDGE('',*,*,#5007,.F.);
#6473=ORIENTED_EDGE('',*,*,#5008,.T.);
#6474=ORIENTED_EDGE('',*,*,#5009,.F.);
#6475=ORIENTED_EDGE('',*,*,#5008,.F.);
#6476=ORIENTED_EDGE('',*,*,#5010,.F.);
#6477=ORIENTED_EDGE('',*,*,#5011,.T.);
#6478=ORIENTED_EDGE('',*,*,#5012,.F.);
#6479=ORIENTED_EDGE('',*,*,#5011,.F.);
#6480=ORIENTED_EDGE('',*,*,#5013,.F.);
#6481=ORIENTED_EDGE('',*,*,#5014,.T.);
#6482=ORIENTED_EDGE('',*,*,#5015,.T.);
#6483=ORIENTED_EDGE('',*,*,#5014,.F.);
#6484=ORIENTED_EDGE('',*,*,#5015,.F.);
#6485=ORIENTED_EDGE('',*,*,#5016,.F.);
#6486=ORIENTED_EDGE('',*,*,#5017,.F.);
#6487=ORIENTED_EDGE('',*,*,#5018,.T.);
#6488=ORIENTED_EDGE('',*,*,#5016,.T.);
#6489=ORIENTED_EDGE('',*,*,#5018,.F.);
#6490=ORIENTED_EDGE('',*,*,#5019,.F.);
#6491=ORIENTED_EDGE('',*,*,#5020,.T.);
#6492=ORIENTED_EDGE('',*,*,#5021,.T.);
#6493=ORIENTED_EDGE('',*,*,#5020,.F.);
#6494=ORIENTED_EDGE('',*,*,#5019,.T.);
#6495=ORIENTED_EDGE('',*,*,#5017,.T.);
#6496=ORIENTED_EDGE('',*,*,#5012,.T.);
#6497=ORIENTED_EDGE('',*,*,#5009,.T.);
#6498=ORIENTED_EDGE('',*,*,#5006,.T.);
#6499=ORIENTED_EDGE('',*,*,#5003,.T.);
#6500=ORIENTED_EDGE('',*,*,#5021,.F.);
#6501=ORIENTED_EDGE('',*,*,#5013,.T.);
#6502=ORIENTED_EDGE('',*,*,#5010,.T.);
#6503=ORIENTED_EDGE('',*,*,#5007,.T.);
#6504=ORIENTED_EDGE('',*,*,#5004,.T.);
#6505=ORIENTED_EDGE('',*,*,#5001,.T.);
#7629=CYLINDRICAL_SURFACE('',#9150,0.225);
#7630=CYLINDRICAL_SURFACE('',#9153,0.225);
#7631=CYLINDRICAL_SURFACE('',#9156,0.225);
#7632=CYLINDRICAL_SURFACE('',#9159,0.225);
#7633=CYLINDRICAL_SURFACE('',#9162,1.59);
#7634=CYLINDRICAL_SURFACE('',#9167,1.2);
#7635=CYLINDRICAL_SURFACE('',#9169,2.4);
#7892=ADVANCED_FACE('',(#1400),#7629,.F.);
#7893=ADVANCED_FACE('',(#1401),#7630,.F.);
#7894=ADVANCED_FACE('',(#1402),#7631,.F.);
#7895=ADVANCED_FACE('',(#1403),#7632,.F.);
#7896=ADVANCED_FACE('',(#1404),#7633,.T.);
#7897=ADVANCED_FACE('',(#1405,#884),#1045,.F.);
#7898=ADVANCED_FACE('',(#1406),#7634,.F.);
#7899=ADVANCED_FACE('',(#1407),#7635,.T.);
#7900=ADVANCED_FACE('',(#1408,#885,#886,#887,#888,#889),#1046,.T.);
#7901=ADVANCED_FACE('',(#1409,#890,#891,#892,#893,#894),#1047,.F.);
#8181=CLOSED_SHELL('',(#7892,#7893,#7894,#7895,#7896,#7897,#7898,#7899,
#7900,#7901));
#9149=AXIS2_PLACEMENT_3D('',#13359,#10854,#10855);
#9150=AXIS2_PLACEMENT_3D('',#13360,#10856,#10857);
#9151=AXIS2_PLACEMENT_3D('',#13362,#10858,#10859);
#9152=AXIS2_PLACEMENT_3D('',#13365,#10861,#10862);
#9153=AXIS2_PLACEMENT_3D('',#13366,#10863,#10864);
#9154=AXIS2_PLACEMENT_3D('',#13368,#10865,#10866);
#9155=AXIS2_PLACEMENT_3D('',#13371,#10868,#10869);
#9156=AXIS2_PLACEMENT_3D('',#13372,#10870,#10871);
#9157=AXIS2_PLACEMENT_3D('',#13374,#10872,#10873);
#9158=AXIS2_PLACEMENT_3D('',#13377,#10875,#10876);
#9159=AXIS2_PLACEMENT_3D('',#13378,#10877,#10878);
#9160=AXIS2_PLACEMENT_3D('',#13380,#10879,#10880);
#9161=AXIS2_PLACEMENT_3D('',#13383,#10882,#10883);
#9162=AXIS2_PLACEMENT_3D('',#13384,#10884,#10885);
#9163=AXIS2_PLACEMENT_3D('',#13386,#10886,#10887);
#9164=AXIS2_PLACEMENT_3D('',#13389,#10889,#10890);
#9165=AXIS2_PLACEMENT_3D('',#13390,#10891,#10892);
#9166=AXIS2_PLACEMENT_3D('',#13392,#10893,#10894);
#9167=AXIS2_PLACEMENT_3D('',#13393,#10895,#10896);
#9168=AXIS2_PLACEMENT_3D('',#13395,#10897,#10898);
#9169=AXIS2_PLACEMENT_3D('',#13397,#10900,#10901);
#9170=AXIS2_PLACEMENT_3D('',#13399,#10902,#10903);
#9171=AXIS2_PLACEMENT_3D('',#13402,#10905,#10906);
#9172=AXIS2_PLACEMENT_3D('',#13403,#10907,#10908);
#9173=AXIS2_PLACEMENT_3D('',#13404,#10909,#10910);
#10854=DIRECTION('axis',(0.,0.,1.));
#10855=DIRECTION('refdir',(1.,0.,0.));
#10856=DIRECTION('center_axis',(1.,0.,0.));
#10857=DIRECTION('ref_axis',(0.,0.,-1.));
#10858=DIRECTION('center_axis',(1.,0.,0.));
#10859=DIRECTION('ref_axis',(0.,0.,-1.));
#10860=DIRECTION('',(1.,0.,0.));
#10861=DIRECTION('center_axis',(-1.,0.,0.));
#10862=DIRECTION('ref_axis',(0.,0.,-1.));
#10863=DIRECTION('center_axis',(1.,0.,0.));
#10864=DIRECTION('ref_axis',(0.,0.,-1.));
#10865=DIRECTION('center_axis',(1.,0.,0.));
#10866=DIRECTION('ref_axis',(0.,0.,-1.));
#10867=DIRECTION('',(1.,0.,0.));
#10868=DIRECTION('center_axis',(-1.,0.,0.));
#10869=DIRECTION('ref_axis',(0.,0.,-1.));
#10870=DIRECTION('center_axis',(1.,0.,0.));
#10871=DIRECTION('ref_axis',(0.,0.,-1.));
#10872=DIRECTION('center_axis',(1.,0.,0.));
#10873=DIRECTION('ref_axis',(0.,0.,-1.));
#10874=DIRECTION('',(1.,0.,0.));
#10875=DIRECTION('center_axis',(-1.,0.,0.));
#10876=DIRECTION('ref_axis',(0.,0.,-1.));
#10877=DIRECTION('center_axis',(1.,0.,0.));
#10878=DIRECTION('ref_axis',(0.,0.,-1.));
#10879=DIRECTION('center_axis',(1.,0.,0.));
#10880=DIRECTION('ref_axis',(0.,0.,-1.));
#10881=DIRECTION('',(1.,0.,0.));
#10882=DIRECTION('center_axis',(-1.,0.,0.));
#10883=DIRECTION('ref_axis',(0.,0.,-1.));
#10884=DIRECTION('center_axis',(1.,0.,0.));
#10885=DIRECTION('ref_axis',(0.,0.,-1.));
#10886=DIRECTION('center_axis',(1.,0.,0.));
#10887=DIRECTION('ref_axis',(0.,0.,-1.));
#10888=DIRECTION('',(-1.,0.,0.));
#10889=DIRECTION('center_axis',(1.,0.,0.));
#10890=DIRECTION('ref_axis',(0.,0.,-1.));
#10891=DIRECTION('center_axis',(1.,0.,0.));
#10892=DIRECTION('ref_axis',(0.,0.,-1.));
#10893=DIRECTION('center_axis',(-1.,0.,0.));
#10894=DIRECTION('ref_axis',(0.,0.,-1.));
#10895=DIRECTION('center_axis',(1.,0.,0.));
#10896=DIRECTION('ref_axis',(0.,0.,-1.));
#10897=DIRECTION('center_axis',(-1.,0.,0.));
#10898=DIRECTION('ref_axis',(0.,0.,-1.));
#10899=DIRECTION('',(-1.,0.,0.));
#10900=DIRECTION('center_axis',(1.,0.,0.));
#10901=DIRECTION('ref_axis',(0.,0.,-1.));
#10902=DIRECTION('center_axis',(1.,0.,0.));
#10903=DIRECTION('ref_axis',(0.,0.,-1.));
#10904=DIRECTION('',(-1.,0.,0.));
#10905=DIRECTION('center_axis',(1.,0.,0.));
#10906=DIRECTION('ref_axis',(0.,0.,-1.));
#10907=DIRECTION('center_axis',(1.,0.,0.));
#10908=DIRECTION('ref_axis',(0.,0.,-1.));
#10909=DIRECTION('center_axis',(1.,0.,0.));
#10910=DIRECTION('ref_axis',(0.,0.,-1.));
#13359=CARTESIAN_POINT('',(0.,0.,0.));
#13360=CARTESIAN_POINT('Origin',(6.2,1.51507575950825,5.51507575950825));
#13361=CARTESIAN_POINT('',(6.3,1.51507575950825,5.74007575950825));
#13362=CARTESIAN_POINT('Origin',(6.3,1.51507575950825,5.51507575950825));
#13363=CARTESIAN_POINT('',(6.5,1.51507575950825,5.74007575950825));
#13364=CARTESIAN_POINT('',(6.2,1.51507575950825,5.74007575950825));
#13365=CARTESIAN_POINT('Origin',(6.5,1.51507575950825,5.51507575950825));
#13366=CARTESIAN_POINT('Origin',(6.2,1.51507575950825,8.48492424049175));
#13367=CARTESIAN_POINT('',(6.3,1.51507575950825,8.70992424049175));
#13368=CARTESIAN_POINT('Origin',(6.3,1.51507575950825,8.48492424049175));
#13369=CARTESIAN_POINT('',(6.5,1.51507575950825,8.70992424049175));
#13370=CARTESIAN_POINT('',(6.2,1.51507575950825,8.70992424049175));
#13371=CARTESIAN_POINT('Origin',(6.5,1.51507575950825,8.48492424049175));
#13372=CARTESIAN_POINT('Origin',(6.2,4.48492424049175,8.48492424049175));
#13373=CARTESIAN_POINT('',(6.3,4.48492424049175,8.70992424049175));
#13374=CARTESIAN_POINT('Origin',(6.3,4.48492424049175,8.48492424049175));
#13375=CARTESIAN_POINT('',(6.5,4.48492424049175,8.70992424049175));
#13376=CARTESIAN_POINT('',(6.2,4.48492424049175,8.70992424049175));
#13377=CARTESIAN_POINT('Origin',(6.5,4.48492424049175,8.48492424049175));
#13378=CARTESIAN_POINT('Origin',(6.2,4.48492424049175,5.51507575950825));
#13379=CARTESIAN_POINT('',(6.3,4.48492424049175,5.74007575950825));
#13380=CARTESIAN_POINT('Origin',(6.3,4.48492424049175,5.51507575950825));
#13381=CARTESIAN_POINT('',(6.5,4.48492424049175,5.74007575950825));
#13382=CARTESIAN_POINT('',(6.2,4.48492424049175,5.74007575950825));
#13383=CARTESIAN_POINT('Origin',(6.5,4.48492424049175,5.51507575950825));
#13384=CARTESIAN_POINT('Origin',(6.,3.,7.));
#13385=CARTESIAN_POINT('',(6.3,3.,8.59));
#13386=CARTESIAN_POINT('Origin',(6.3,3.,7.));
#13387=CARTESIAN_POINT('',(6.,3.,8.59));
#13388=CARTESIAN_POINT('',(6.,3.,8.59));
#13389=CARTESIAN_POINT('Origin',(6.,3.,7.));
#13390=CARTESIAN_POINT('Origin',(6.,3.,7.));
#13391=CARTESIAN_POINT('',(6.,3.,8.2));
#13392=CARTESIAN_POINT('Origin',(6.,3.,7.));
#13393=CARTESIAN_POINT('Origin',(6.3,3.,7.));
#13394=CARTESIAN_POINT('',(6.5,3.,8.2));
#13395=CARTESIAN_POINT('Origin',(6.5,3.,7.));
#13396=CARTESIAN_POINT('',(6.3,3.,8.2));
#13397=CARTESIAN_POINT('Origin',(6.3,3.,7.));
#13398=CARTESIAN_POINT('',(6.5,3.,9.4));
#13399=CARTESIAN_POINT('Origin',(6.5,3.,7.));
#13400=CARTESIAN_POINT('',(6.3,3.,9.4));
#13401=CARTESIAN_POINT('',(6.3,3.,9.4));
#13402=CARTESIAN_POINT('Origin',(6.3,3.,7.));
#13403=CARTESIAN_POINT('Origin',(6.5,3.,7.));
#13404=CARTESIAN_POINT('Origin',(6.3,3.,7.));
#16958=UNCERTAINTY_MEASURE_WITH_UNIT(LENGTH_MEASURE(0.001),#17047,
'DISTANCE_ACCURACY_VALUE',
'Maximum model space distance between geometric entities at asserted c
onnectivities');
#16993=UNCERTAINTY_MEASURE_WITH_UNIT(LENGTH_MEASURE(0.001),#17047,
'DISTANCE_ACCURACY_VALUE',
'Maximum model space distance between geometric entities at asserted c
onnectivities');
#17011=(
GEOMETRIC_REPRESENTATION_CONTEXT(3)
GLOBAL_UNCERTAINTY_ASSIGNED_CONTEXT((#16958))
GLOBAL_UNIT_ASSIGNED_CONTEXT((#17047,#17049,#17050))
REPRESENTATION_CONTEXT('','3D')
);
#17046=(
GEOMETRIC_REPRESENTATION_CONTEXT(3)
GLOBAL_UNCERTAINTY_ASSIGNED_CONTEXT((#16993))
GLOBAL_UNIT_ASSIGNED_CONTEXT((#17047,#17049,#17050))
REPRESENTATION_CONTEXT('','3D')
);
#17047=(
LENGTH_UNIT()
NAMED_UNIT(*)
SI_UNIT(.CENTI.,.METRE.)
);
#17049=(
NAMED_UNIT(*)
PLANE_ANGLE_UNIT()
SI_UNIT($,.RADIAN.)
);
#17050=(
NAMED_UNIT(*)
SI_UNIT($,.STERADIAN.)
SOLID_ANGLE_UNIT()
);
#17068=SHAPE_DEFINITION_REPRESENTATION(#17120,#17275);
#17120=PRODUCT_DEFINITION_SHAPE('',$,#17328);
#17275=SHAPE_REPRESENTATION('',(#9149),#17011);
#17310=PRODUCT_DEFINITION_CONTEXT('part definition',#17468,'design');
#17328=PRODUCT_DEFINITION('Bearing cap (7)','Bearing cap (7)',#17380,#17310);
#17380=PRODUCT_DEFINITION_FORMATION('',$,#17487);
#17468=APPLICATION_CONTEXT(
'Core Data for Automotive Mechanical Design Process');
#17469=PRODUCT_CONTEXT('part definition',#17468,'mechanical');
#17487=PRODUCT('Bearing cap (7)','Bearing cap (7)','Bearing cap (7)',(#17469));
#17585=COLOUR_RGB('Grey',0.48,0.52,0.57);
#17586=FILL_AREA_STYLE_COLOUR('',#17585);
#17587=FILL_AREA_STYLE('',(#17586));
#17588=SURFACE_STYLE_FILL_AREA(#17587);
#17589=SURFACE_SIDE_STYLE('',(#17588));
#17590=SURFACE_STYLE_USAGE(.BOTH.,#17589);
#17591=PRESENTATION_STYLE_ASSIGNMENT((#17590));
ENDSEC;
END-ISO-10303-21;
